ISO-10303-21;
HEADER;
/* Generated by software containing ST-Developer
 * from STEP Tools, Inc. (www.steptools.com) 
 */

FILE_DESCRIPTION(
/* description */ ('Bin tilter linkage'),
/* implementation_level */ '2;1');

FILE_NAME(
/* name */ 'Cradle rim (1).step',
/* time_stamp */ '2026-10-28T03:26:24-07:00',
/* author */ (''),
/* organization */ (''),
/* preprocessor_version */ 'ST-DEVELOPER v20.2',
/* originating_system */ 'Autodesk Translation Framework v15.17.0.0',
/* authorisation */ '');

FILE_SCHEMA (('AUTOMOTIVE_DESIGN { 1 0 10303 214 3 1 1 }'));
ENDSEC;

DATA;
#10=MECHANICAL_DESIGN_GEOMETRIC_PRESENTATION_REPRESENTATION('',(#949),#23728);
#729=SHAPE_REPRESENTATION_RELATIONSHIP('SRR','None',#24197,#835);
#835=ADVANCED_BREP_SHAPE_REPRESENTATION('',(#1062),#23697);
#949=STYLED_ITEM('',(#24758),#1062);
#1062=MANIFOLD_SOLID_BREP('Body1',#12480);
#1775=PLANE('',#15006);
#1776=PLANE('',#15007);
#1777=PLANE('',#15008);
#1778=PLANE('',#15009);
#1779=PLANE('',#15010);
#1780=PLANE('',#15011);
#2476=FACE_OUTER_BOUND('',#3577,.T.);
#2477=FACE_OUTER_BOUND('',#3578,.T.);
#2478=FACE_OUTER_BOUND('',#3579,.T.);
#2479=FACE_OUTER_BOUND('',#3580,.T.);
#2480=FACE_OUTER_BOUND('',#3581,.T.);
#2481=FACE_OUTER_BOUND('',#3582,.T.);
#3577=EDGE_LOOP('',(#10573,#10574,#10575,#10576));
#3578=EDGE_LOOP('',(#10577,#10578,#10579,#10580));
#3579=EDGE_LOOP('',(#10581,#10582,#10583,#10584));
#3580=EDGE_LOOP('',(#10585,#10586,#10587,#10588));
#3581=EDGE_LOOP('',(#10589,#10590,#10591,#10592));
#3582=EDGE_LOOP('',(#10593,#10594,#10595,#10596));
#4328=LINE('',#22605,#5003);
#4329=LINE('',#22607,#5004);
#4330=LINE('',#22609,#5005);
#4331=LINE('',#22610,#5006);
#4332=LINE('',#22613,#5007);
#4333=LINE('',#22615,#5008);
#4334=LINE('',#22616,#5009);
#4335=LINE('',#22619,#5010);
#4336=LINE('',#22621,#5011);
#4337=LINE('',#22622,#5012);
#4338=LINE('',#22624,#5013);
#4339=LINE('',#22625,#5014);
#5003=VECTOR('',#18615,1.);
#5004=VECTOR('',#18616,1.);
#5005=VECTOR('',#18617,1.);
#5006=VECTOR('',#18618,1.);
#5007=VECTOR('',#18621,1.);
#5008=VECTOR('',#18622,1.);
#5009=VECTOR('',#18623,1.);
#5010=VECTOR('',#18626,1.);
#5011=VECTOR('',#18627,1.);
#5012=VECTOR('',#18628,1.);
#5013=VECTOR('',#18631,1.);
#5014=VECTOR('',#18632,1.);
#6697=VERTEX_POINT('',#22603);
#6698=VERTEX_POINT('',#22604);
#6699=VERTEX_POINT('',#22606);
#6700=VERTEX_POINT('',#22608);
#6701=VERTEX_POINT('',#22612);
#6702=VERTEX_POINT('',#22614);
#6703=VERTEX_POINT('',#22618);
#6704=VERTEX_POINT('',#22620);
#8026=EDGE_CURVE('',#6697,#6698,#4328,.T.);
#8027=EDGE_CURVE('',#6698,#6699,#4329,.T.);
#8028=EDGE_CURVE('',#6700,#6699,#4330,.T.);
#8029=EDGE_CURVE('',#6697,#6700,#4331,.T.);
#8030=EDGE_CURVE('',#6701,#6697,#4332,.T.);
#8031=EDGE_CURVE('',#6702,#6700,#4333,.T.);
#8032=EDGE_CURVE('',#6701,#6702,#4334,.T.);
#8033=EDGE_CURVE('',#6703,#6701,#4335,.T.);
#8034=EDGE_CURVE('',#6704,#6702,#4336,.T.);
#8035=EDGE_CURVE('',#6703,#6704,#4337,.T.);
#8036=EDGE_CURVE('',#6698,#6703,#4338,.T.);
#8037=EDGE_CURVE('',#6699,#6704,#4339,.T.);
#10573=ORIENTED_EDGE('',*,*,#8026,.T.);
#10574=ORIENTED_EDGE('',*,*,#8027,.T.);
#10575=ORIENTED_EDGE('',*,*,#8028,.F.);
#10576=ORIENTED_EDGE('',*,*,#8029,.F.);
#10577=ORIENTED_EDGE('',*,*,#8030,.T.);
#10578=ORIENTED_EDGE('',*,*,#8029,.T.);
#10579=ORIENTED_EDGE('',*,*,#8031,.F.);
#10580=ORIENTED_EDGE('',*,*,#8032,.F.);
#10581=ORIENTED_EDGE('',*,*,#8033,.T.);
#10582=ORIENTED_EDGE('',*,*,#8032,.T.);
#10583=ORIENTED_EDGE('',*,*,#8034,.F.);
#10584=ORIENTED_EDGE('',*,*,#8035,.F.);
#10585=ORIENTED_EDGE('',*,*,#8036,.T.);
#10586=ORIENTED_EDGE('',*,*,#8035,.T.);
#10587=ORIENTED_EDGE('',*,*,#8037,.F.);
#10588=ORIENTED_EDGE('',*,*,#8027,.F.);
#10589=ORIENTED_EDGE('',*,*,#8037,.T.);
#10590=ORIENTED_EDGE('',*,*,#8034,.T.);
#10591=ORIENTED_EDGE('',*,*,#8031,.T.);
#10592=ORIENTED_EDGE('',*,*,#8028,.T.);
#10593=ORIENTED_EDGE('',*,*,#8036,.F.);
#10594=ORIENTED_EDGE('',*,*,#8026,.F.);
#10595=ORIENTED_EDGE('',*,*,#8030,.F.);
#10596=ORIENTED_EDGE('',*,*,#8033,.F.);
#12201=ADVANCED_FACE('',(#2476),#1775,.T.);
#12202=ADVANCED_FACE('',(#2477),#1776,.T.);
#12203=ADVANCED_FACE('',(#2478),#1777,.T.);
#12204=ADVANCED_FACE('',(#2479),#1778,.T.);
#12205=ADVANCED_FACE('',(#2480),#1779,.T.);
#12206=ADVANCED_FACE('',(#2481),#1780,.F.);
#12480=CLOSED_SHELL('',(#12201,#12202,#12203,#12204,#12205,#12206));
#15005=AXIS2_PLACEMENT_3D('',#22601,#18611,#18612);
#15006=AXIS2_PLACEMENT_3D('',#22602,#18613,#18614);
#15007=AXIS2_PLACEMENT_3D('',#22611,#18619,#18620);
#15008=AXIS2_PLACEMENT_3D('',#22617,#18624,#18625);
#15009=AXIS2_PLACEMENT_3D('',#22623,#18629,#18630);
#15010=AXIS2_PLACEMENT_3D('',#22626,#18633,#18634);
#15011=AXIS2_PLACEMENT_3D('',#22627,#18635,#18636);
#18611=DIRECTION('axis',(0.,0.,1.));
#18612=DIRECTION('refdir',(1.,0.,0.));
#18613=DIRECTION('center_axis',(0.,1.,0.));
#18614=DIRECTION('ref_axis',(-1.,0.,0.));
#18615=DIRECTION('',(-1.,0.,0.));
#18616=DIRECTION('',(0.,0.,1.));
#18617=DIRECTION('',(-1.,0.,0.));
#18618=DIRECTION('',(0.,0.,1.));
#18619=DIRECTION('center_axis',(1.,0.,0.));
#18620=DIRECTION('ref_axis',(0.,1.,0.));
#18621=DIRECTION('',(0.,1.,0.));
#18622=DIRECTION('',(0.,1.,0.));
#18623=DIRECTION('',(0.,0.,1.));
#18624=DIRECTION('center_axis',(0.,-1.,0.));
#18625=DIRECTION('ref_axis',(1.,0.,0.));
#18626=DIRECTION('',(1.,0.,0.));
#18627=DIRECTION('',(1.,0.,0.));
#18628=DIRECTION('',(0.,0.,1.));
#18629=DIRECTION('center_axis',(-1.,0.,0.));
#18630=DIRECTION('ref_axis',(0.,-1.,0.));
#18631=DIRECTION('',(0.,-1.,0.));
#18632=DIRECTION('',(0.,-1.,0.));
#18633=DIRECTION('center_axis',(0.,0.,1.));
#18634=DIRECTION('ref_axis',(1.,0.,0.));
#18635=DIRECTION('center_axis',(0.,0.,1.));
#18636=DIRECTION('ref_axis',(1.,0.,0.));
#22601=CARTESIAN_POINT('',(0.,0.,0.));
#22602=CARTESIAN_POINT('Origin',(28.,7.5,32.8));
#22603=CARTESIAN_POINT('',(28.,7.5,32.8));
#22604=CARTESIAN_POINT('',(27.2,7.5,32.8));
#22605=CARTESIAN_POINT('',(28.,7.5,32.8));
#22606=CARTESIAN_POINT('',(27.2,7.5,35.3));
#22607=CARTESIAN_POINT('',(27.2,7.5,32.8));
#22608=CARTESIAN_POINT('',(28.,7.5,35.3));
#22609=CARTESIAN_POINT('',(28.,7.5,35.3));
#22610=CARTESIAN_POINT('',(28.,7.5,32.8));
#22611=CARTESIAN_POINT('Origin',(28.,-3.5,32.8));
#22612=CARTESIAN_POINT('',(28.,-3.5,32.8));
#22613=CARTESIAN_POINT('',(28.,-3.5,32.8));
#22614=CARTESIAN_POINT('',(28.,-3.5,35.3));
#22615=CARTESIAN_POINT('',(28.,-3.5,35.3));
#22616=CARTESIAN_POINT('',(28.,-3.5,32.8));
#22617=CARTESIAN_POINT('Origin',(27.2,-3.5,32.8));
#22618=CARTESIAN_POINT('',(27.2,-3.5,32.8));
#22619=CARTESIAN_POINT('',(27.2,-3.5,32.8));
#22620=CARTESIAN_POINT('',(27.2,-3.5,35.3));
#22621=CARTESIAN_POINT('',(27.2,-3.5,35.3));
#22622=CARTESIAN_POINT('',(27.2,-3.5,32.8));
#22623=CARTESIAN_POINT('Origin',(27.2,7.5,32.8));
#22624=CARTESIAN_POINT('',(27.2,7.5,32.8));
#22625=CARTESIAN_POINT('',(27.2,7.5,35.3));
#22626=CARTESIAN_POINT('Origin',(27.6,2.,35.3));
#22627=CARTESIAN_POINT('Origin',(27.6,2.,32.8));
#23580=UNCERTAINTY_MEASURE_WITH_UNIT(LENGTH_MEASURE(0.001),#23729,
'DISTANCE_ACCURACY_VALUE',
'Maximum model space distance between geometric entities at asserted c
onnectivities');
#23611=UNCERTAINTY_MEASURE_WITH_UNIT(LENGTH_MEASURE(0.001),#23729,
'DISTANCE_ACCURACY_VALUE',
'Maximum model space distance between geometric entities at asserted c
onnectivities');
#23697=(
GEOMETRIC_REPRESENTATION_CONTEXT(3)
GLOBAL_UNCERTAINTY_ASSIGNED_CONTEXT((#23580))
GLOBAL_UNIT_ASSIGNED_CONTEXT((#23729,#23731,#23732))
REPRESENTATION_CONTEXT('','3D')
);
#23728=(
GEOMETRIC_REPRESENTATION_CONTEXT(3)
GLOBAL_UNCERTAINTY_ASSIGNED_CONTEXT((#23611))
GLOBAL_UNIT_ASSIGNED_CONTEXT((#23729,#23731,#23732))
REPRESENTATION_CONTEXT('','3D')
);
#23729=(
LENGTH_UNIT()
NAMED_UNIT(*)
SI_UNIT(.CENTI.,.METRE.)
);
#23731=(
NAMED_UNIT(*)
PLANE_ANGLE_UNIT()
SI_UNIT($,.RADIAN.)
);
#23732=(
NAMED_UNIT(*)
SI_UNIT($,.STERADIAN.)
SOLID_ANGLE_UNIT()
);
#23818=SHAPE_DEFINITION_REPRESENTATION(#23985,#24197);
#23985=PRODUCT_DEFINITION_SHAPE('',$,#24314);
#24197=SHAPE_REPRESENTATION('',(#15005),#23697);
#24228=PRODUCT_DEFINITION_CONTEXT('part definition',#24578,'design');
#24314=PRODUCT_DEFINITION('Cradle rim (1)','Cradle rim (1)',#24430,#24228);
#24430=PRODUCT_DEFINITION_FORMATION('',$,#24665);
#24578=APPLICATION_CONTEXT(
'Core Data for Automotive Mechanical Design Process');
#24579=PRODUCT_CONTEXT('part definition',#24578,'mechanical');
#24665=PRODUCT('Cradle rim (1)','Cradle rim (1)','Cradle rim (1)',(#24579));
#24752=COLOUR_RGB('Sky Blue',0.24,0.69,0.87);
#24753=FILL_AREA_STYLE_COLOUR('',#24752);
#24754=FILL_AREA_STYLE('',(#24753));
#24755=SURFACE_STYLE_FILL_AREA(#24754);
#24756=SURFACE_SIDE_STYLE('',(#24755));
#24757=SURFACE_STYLE_USAGE(.BOTH.,#24756);
#24758=PRESENTATION_STYLE_ASSIGNMENT((#24757));
ENDSEC;
END-ISO-10303-21;
